ISO-10303-21;
HEADER;
/* Generated by software containing ST-Developer
 * from STEP Tools, Inc. (www.steptools.com) 
 */

FILE_DESCRIPTION(
/* description */ (''),
/* implementation_level */ '2;1');

FILE_NAME(
/* name */ 'Motor.step',
/* time_stamp */ '2026-10-22T16:03:28+06:00',
/* author */ (''),
/* organization */ (''),
/* preprocessor_version */ 'ST-DEVELOPER v20.2',
/* originating_system */ 'Autodesk Translation Framework v15.15.0.0',
/* authorisation */ '');

FILE_SCHEMA (('AUTOMOTIVE_DESIGN { 1 0 10303 214 3 1 1 }'));
ENDSEC;

DATA;
#10=MECHANICAL_DESIGN_GEOMETRIC_PRESENTATION_REPRESENTATION('',(#87),#6096);
#65=SHAPE_REPRESENTATION_RELATIONSHIP('SRR','None',#6140,#76);
#76=ADVANCED_BREP_SHAPE_REPRESENTATION('',(#98),#6088);
#87=STYLED_ITEM('',(#6269),#98);
#98=MANIFOLD_SOLID_BREP('Motor',#3596);
#223=PLANE('',#3860);
#224=PLANE('',#3864);
#225=PLANE('',#3869);
#226=PLANE('',#3872);
#227=PLANE('',#3873);
#228=PLANE('',#3874);
#380=FACE_OUTER_BOUND('',#581,.T.);
#381=FACE_OUTER_BOUND('',#582,.T.);
#382=FACE_OUTER_BOUND('',#583,.T.);
#383=FACE_OUTER_BOUND('',#584,.T.);
#384=FACE_OUTER_BOUND('',#585,.T.);
#385=FACE_OUTER_BOUND('',#586,.T.);
#386=FACE_OUTER_BOUND('',#587,.T.);
#387=FACE_OUTER_BOUND('',#588,.T.);
#388=FACE_OUTER_BOUND('',#589,.T.);
#389=FACE_OUTER_BOUND('',#590,.T.);
#581=EDGE_LOOP('',(#2852,#2853,#2854,#2855));
#582=EDGE_LOOP('',(#2856,#2857,#2858,#2859,#2860,#2861,#2862,#2863));
#583=EDGE_LOOP('',(#2864,#2865,#2866,#2867));
#584=EDGE_LOOP('',(#2868,#2869,#2870,#2871));
#585=EDGE_LOOP('',(#2872,#2873,#2874,#2875));
#586=EDGE_LOOP('',(#2876,#2877,#2878,#2879));
#587=EDGE_LOOP('',(#2880,#2881,#2882,#2883));
#588=EDGE_LOOP('',(#2884,#2885,#2886,#2887));
#589=EDGE_LOOP('',(#2888,#2889,#2890,#2891));
#590=EDGE_LOOP('',(#2892,#2893,#2894,#2895,#2896,#2897,#2898,#2899));
#911=LINE('',#5527,#1290);
#912=LINE('',#5530,#1291);
#913=LINE('',#5533,#1292);
#914=LINE('',#5537,#1293);
#915=LINE('',#5541,#1294);
#916=LINE('',#5544,#1295);
#917=LINE('',#5547,#1296);
#918=LINE('',#5548,#1297);
#919=LINE('',#5552,#1298);
#920=LINE('',#5557,#1299);
#921=LINE('',#5558,#1300);
#922=LINE('',#5561,#1301);
#923=LINE('',#5562,#1302);
#924=LINE('',#5566,#1303);
#925=LINE('',#5568,#1304);
#926=LINE('',#5570,#1305);
#1290=VECTOR('',#4494,10.);
#1291=VECTOR('',#4497,10.);
#1292=VECTOR('',#4500,10.);
#1293=VECTOR('',#4503,10.);
#1294=VECTOR('',#4506,10.);
#1295=VECTOR('',#4509,10.);
#1296=VECTOR('',#4512,10.);
#1297=VECTOR('',#4513,10.);
#1298=VECTOR('',#4518,10.);
#1299=VECTOR('',#4523,10.);
#1300=VECTOR('',#4524,10.);
#1301=VECTOR('',#4527,10.);
#1302=VECTOR('',#4528,10.);
#1303=VECTOR('',#4533,10.);
#1304=VECTOR('',#4536,10.);
#1305=VECTOR('',#4539,10.);
#1528=CIRCLE('',#3858,5.);
#1529=CIRCLE('',#3859,5.);
#1530=CIRCLE('',#3861,5.);
#1531=CIRCLE('',#3862,5.);
#1532=CIRCLE('',#3863,5.);
#1533=CIRCLE('',#3866,5.);
#1534=CIRCLE('',#3868,5.);
#1535=CIRCLE('',#3871,5.);
#1740=VERTEX_POINT('',#5523);
#1741=VERTEX_POINT('',#5524);
#1742=VERTEX_POINT('',#5526);
#1743=VERTEX_POINT('',#5528);
#1744=VERTEX_POINT('',#5532);
#1745=VERTEX_POINT('',#5534);
#1746=VERTEX_POINT('',#5536);
#1747=VERTEX_POINT('',#5538);
#1748=VERTEX_POINT('',#5540);
#1749=VERTEX_POINT('',#5542);
#1750=VERTEX_POINT('',#5546);
#1751=VERTEX_POINT('',#5550);
#1752=VERTEX_POINT('',#5554);
#1753=VERTEX_POINT('',#5555);
#1754=VERTEX_POINT('',#5560);
#1755=VERTEX_POINT('',#5564);
#2138=EDGE_CURVE('',#1740,#1741,#1528,.T.);
#2139=EDGE_CURVE('',#1741,#1742,#911,.T.);
#2140=EDGE_CURVE('',#1742,#1743,#1529,.T.);
#2141=EDGE_CURVE('',#1743,#1740,#912,.T.);
#2142=EDGE_CURVE('',#1744,#1742,#913,.T.);
#2143=EDGE_CURVE('',#1745,#1744,#1530,.T.);
#2144=EDGE_CURVE('',#1746,#1745,#914,.T.);
#2145=EDGE_CURVE('',#1747,#1746,#1531,.T.);
#2146=EDGE_CURVE('',#1748,#1747,#915,.T.);
#2147=EDGE_CURVE('',#1749,#1748,#1532,.T.);
#2148=EDGE_CURVE('',#1743,#1749,#916,.T.);
#2149=EDGE_CURVE('',#1750,#1741,#917,.T.);
#2150=EDGE_CURVE('',#1744,#1750,#918,.T.);
#2151=EDGE_CURVE('',#1750,#1751,#1533,.T.);
#2152=EDGE_CURVE('',#1751,#1745,#919,.T.);
#2153=EDGE_CURVE('',#1752,#1753,#1534,.T.);
#2154=EDGE_CURVE('',#1753,#1749,#920,.T.);
#2155=EDGE_CURVE('',#1748,#1752,#921,.T.);
#2156=EDGE_CURVE('',#1754,#1747,#922,.T.);
#2157=EDGE_CURVE('',#1752,#1754,#923,.T.);
#2158=EDGE_CURVE('',#1755,#1754,#1535,.T.);
#2159=EDGE_CURVE('',#1746,#1755,#924,.T.);
#2160=EDGE_CURVE('',#1755,#1751,#925,.T.);
#2161=EDGE_CURVE('',#1740,#1753,#926,.T.);
#2852=ORIENTED_EDGE('',*,*,#2138,.T.);
#2853=ORIENTED_EDGE('',*,*,#2139,.T.);
#2854=ORIENTED_EDGE('',*,*,#2140,.T.);
#2855=ORIENTED_EDGE('',*,*,#2141,.T.);
#2856=ORIENTED_EDGE('',*,*,#2140,.F.);
#2857=ORIENTED_EDGE('',*,*,#2142,.F.);
#2858=ORIENTED_EDGE('',*,*,#2143,.F.);
#2859=ORIENTED_EDGE('',*,*,#2144,.F.);
#2860=ORIENTED_EDGE('',*,*,#2145,.F.);
#2861=ORIENTED_EDGE('',*,*,#2146,.F.);
#2862=ORIENTED_EDGE('',*,*,#2147,.F.);
#2863=ORIENTED_EDGE('',*,*,#2148,.F.);
#2864=ORIENTED_EDGE('',*,*,#2139,.F.);
#2865=ORIENTED_EDGE('',*,*,#2149,.F.);
#2866=ORIENTED_EDGE('',*,*,#2150,.F.);
#2867=ORIENTED_EDGE('',*,*,#2142,.T.);
#2868=ORIENTED_EDGE('',*,*,#2151,.T.);
#2869=ORIENTED_EDGE('',*,*,#2152,.T.);
#2870=ORIENTED_EDGE('',*,*,#2143,.T.);
#2871=ORIENTED_EDGE('',*,*,#2150,.T.);
#2872=ORIENTED_EDGE('',*,*,#2153,.T.);
#2873=ORIENTED_EDGE('',*,*,#2154,.T.);
#2874=ORIENTED_EDGE('',*,*,#2147,.T.);
#2875=ORIENTED_EDGE('',*,*,#2155,.T.);
#2876=ORIENTED_EDGE('',*,*,#2155,.F.);
#2877=ORIENTED_EDGE('',*,*,#2146,.T.);
#2878=ORIENTED_EDGE('',*,*,#2156,.F.);
#2879=ORIENTED_EDGE('',*,*,#2157,.F.);
#2880=ORIENTED_EDGE('',*,*,#2158,.T.);
#2881=ORIENTED_EDGE('',*,*,#2156,.T.);
#2882=ORIENTED_EDGE('',*,*,#2145,.T.);
#2883=ORIENTED_EDGE('',*,*,#2159,.T.);
#2884=ORIENTED_EDGE('',*,*,#2152,.F.);
#2885=ORIENTED_EDGE('',*,*,#2160,.F.);
#2886=ORIENTED_EDGE('',*,*,#2159,.F.);
#2887=ORIENTED_EDGE('',*,*,#2144,.T.);
#2888=ORIENTED_EDGE('',*,*,#2141,.F.);
#2889=ORIENTED_EDGE('',*,*,#2148,.T.);
#2890=ORIENTED_EDGE('',*,*,#2154,.F.);
#2891=ORIENTED_EDGE('',*,*,#2161,.F.);
#2892=ORIENTED_EDGE('',*,*,#2138,.F.);
#2893=ORIENTED_EDGE('',*,*,#2161,.T.);
#2894=ORIENTED_EDGE('',*,*,#2153,.F.);
#2895=ORIENTED_EDGE('',*,*,#2157,.T.);
#2896=ORIENTED_EDGE('',*,*,#2158,.F.);
#2897=ORIENTED_EDGE('',*,*,#2160,.T.);
#2898=ORIENTED_EDGE('',*,*,#2151,.F.);
#2899=ORIENTED_EDGE('',*,*,#2149,.T.);
#3379=CYLINDRICAL_SURFACE('',#3857,5.);
#3380=CYLINDRICAL_SURFACE('',#3865,5.);
#3381=CYLINDRICAL_SURFACE('',#3867,5.);
#3382=CYLINDRICAL_SURFACE('',#3870,5.);
#3487=ADVANCED_FACE('',(#380),#3379,.T.);
#3488=ADVANCED_FACE('',(#381),#223,.F.);
#3489=ADVANCED_FACE('',(#382),#224,.T.);
#3490=ADVANCED_FACE('',(#383),#3380,.T.);
#3491=ADVANCED_FACE('',(#384),#3381,.T.);
#3492=ADVANCED_FACE('',(#385),#225,.T.);
#3493=ADVANCED_FACE('',(#386),#3382,.T.);
#3494=ADVANCED_FACE('',(#387),#226,.T.);
#3495=ADVANCED_FACE('',(#388),#227,.T.);
#3496=ADVANCED_FACE('',(#389),#228,.T.);
#3596=CLOSED_SHELL('',(#3487,#3488,#3489,#3490,#3491,#3492,#3493,#3494,
#3495,#3496));
#3856=AXIS2_PLACEMENT_3D('',#5521,#4488,#4489);
#3857=AXIS2_PLACEMENT_3D('',#5522,#4490,#4491);
#3858=AXIS2_PLACEMENT_3D('',#5525,#4492,#4493);
#3859=AXIS2_PLACEMENT_3D('',#5529,#4495,#4496);
#3860=AXIS2_PLACEMENT_3D('',#5531,#4498,#4499);
#3861=AXIS2_PLACEMENT_3D('',#5535,#4501,#4502);
#3862=AXIS2_PLACEMENT_3D('',#5539,#4504,#4505);
#3863=AXIS2_PLACEMENT_3D('',#5543,#4507,#4508);
#3864=AXIS2_PLACEMENT_3D('',#5545,#4510,#4511);
#3865=AXIS2_PLACEMENT_3D('',#5549,#4514,#4515);
#3866=AXIS2_PLACEMENT_3D('',#5551,#4516,#4517);
#3867=AXIS2_PLACEMENT_3D('',#5553,#4519,#4520);
#3868=AXIS2_PLACEMENT_3D('',#5556,#4521,#4522);
#3869=AXIS2_PLACEMENT_3D('',#5559,#4525,#4526);
#3870=AXIS2_PLACEMENT_3D('',#5563,#4529,#4530);
#3871=AXIS2_PLACEMENT_3D('',#5565,#4531,#4532);
#3872=AXIS2_PLACEMENT_3D('',#5567,#4534,#4535);
#3873=AXIS2_PLACEMENT_3D('',#5569,#4537,#4538);
#3874=AXIS2_PLACEMENT_3D('',#5571,#4540,#4541);
#4488=DIRECTION('axis',(0.,0.,1.));
#4489=DIRECTION('refdir',(1.,0.,0.));
#4490=DIRECTION('center_axis',(0.,1.,0.));
#4491=DIRECTION('ref_axis',(-0.707106781186547,0.,-0.707106781186547));
#4492=DIRECTION('center_axis',(0.,-1.,0.));
#4493=DIRECTION('ref_axis',(-0.707106781186547,0.,-0.707106781186547));
#4494=DIRECTION('',(0.,-1.,0.));
#4495=DIRECTION('center_axis',(0.,1.,0.));
#4496=DIRECTION('ref_axis',(-0.707106781186547,0.,-0.707106781186547));
#4497=DIRECTION('',(0.,1.,0.));
#4498=DIRECTION('center_axis',(0.,1.,0.));
#4499=DIRECTION('ref_axis',(-1.,0.,0.));
#4500=DIRECTION('',(-1.,0.,0.));
#4501=DIRECTION('center_axis',(0.,1.,0.));
#4502=DIRECTION('ref_axis',(0.707106781186547,0.,-0.707106781186547));
#4503=DIRECTION('',(0.,0.,-1.));
#4504=DIRECTION('center_axis',(0.,1.,0.));
#4505=DIRECTION('ref_axis',(0.707106781186547,0.,0.707106781186547));
#4506=DIRECTION('',(1.,0.,0.));
#4507=DIRECTION('center_axis',(0.,1.,0.));
#4508=DIRECTION('ref_axis',(-0.707106781186547,0.,0.707106781186547));
#4509=DIRECTION('',(0.,0.,1.));
#4510=DIRECTION('center_axis',(0.,0.,-1.));
#4511=DIRECTION('ref_axis',(-1.,0.,0.));
#4512=DIRECTION('',(-1.,0.,0.));
#4513=DIRECTION('',(0.,1.,0.));
#4514=DIRECTION('center_axis',(0.,1.,0.));
#4515=DIRECTION('ref_axis',(0.707106781186547,0.,-0.707106781186547));
#4516=DIRECTION('center_axis',(0.,-1.,0.));
#4517=DIRECTION('ref_axis',(0.707106781186547,0.,-0.707106781186547));
#4518=DIRECTION('',(0.,-1.,0.));
#4519=DIRECTION('center_axis',(0.,1.,0.));
#4520=DIRECTION('ref_axis',(-0.707106781186547,0.,0.707106781186547));
#4521=DIRECTION('center_axis',(0.,-1.,0.));
#4522=DIRECTION('ref_axis',(-0.707106781186547,0.,0.707106781186547));
#4523=DIRECTION('',(0.,-1.,0.));
#4524=DIRECTION('',(0.,1.,0.));
#4525=DIRECTION('center_axis',(0.,0.,1.));
#4526=DIRECTION('ref_axis',(1.,0.,0.));
#4527=DIRECTION('',(0.,-1.,0.));
#4528=DIRECTION('',(1.,0.,0.));
#4529=DIRECTION('center_axis',(0.,1.,0.));
#4530=DIRECTION('ref_axis',(0.707106781186547,0.,0.707106781186547));
#4531=DIRECTION('center_axis',(0.,-1.,0.));
#4532=DIRECTION('ref_axis',(0.707106781186547,0.,0.707106781186547));
#4533=DIRECTION('',(0.,1.,0.));
#4534=DIRECTION('center_axis',(1.,0.,0.));
#4535=DIRECTION('ref_axis',(0.,0.,-1.));
#4536=DIRECTION('',(0.,0.,-1.));
#4537=DIRECTION('center_axis',(-1.,0.,0.));
#4538=DIRECTION('ref_axis',(0.,0.,1.));
#4539=DIRECTION('',(0.,0.,1.));
#4540=DIRECTION('center_axis',(0.,1.,0.));
#4541=DIRECTION('ref_axis',(0.,0.,1.));
#5521=CARTESIAN_POINT('',(0.,0.,0.));
#5522=CARTESIAN_POINT('Origin',(-25.,600.5,16.5000000000007));
#5523=CARTESIAN_POINT('',(-30.,730.5,16.5000000000007));
#5524=CARTESIAN_POINT('',(-25.,730.5,11.5000000000007));
#5525=CARTESIAN_POINT('Origin',(-25.,730.5,16.5000000000007));
#5526=CARTESIAN_POINT('',(-25.,600.5,11.5000000000007));
#5527=CARTESIAN_POINT('',(-25.,600.5,11.5000000000007));
#5528=CARTESIAN_POINT('',(-30.,600.5,16.5000000000007));
#5529=CARTESIAN_POINT('Origin',(-25.,600.5,16.5000000000007));
#5530=CARTESIAN_POINT('',(-30.,600.5,16.5000000000007));
#5531=CARTESIAN_POINT('Origin',(0.,600.5,41.5000000000007));
#5532=CARTESIAN_POINT('',(25.,600.5,11.5000000000007));
#5533=CARTESIAN_POINT('',(30.,600.5,11.5000000000007));
#5534=CARTESIAN_POINT('',(30.,600.5,16.5000000000007));
#5535=CARTESIAN_POINT('Origin',(25.,600.5,16.5000000000007));
#5536=CARTESIAN_POINT('',(30.,600.5,66.5000000000007));
#5537=CARTESIAN_POINT('',(30.,600.5,71.5000000000007));
#5538=CARTESIAN_POINT('',(25.,600.5,71.5000000000007));
#5539=CARTESIAN_POINT('Origin',(25.,600.5,66.5000000000007));
#5540=CARTESIAN_POINT('',(-25.,600.5,71.5000000000007));
#5541=CARTESIAN_POINT('',(-30.,600.5,71.5000000000007));
#5542=CARTESIAN_POINT('',(-30.,600.5,66.5000000000007));
#5543=CARTESIAN_POINT('Origin',(-25.,600.5,66.5000000000007));
#5544=CARTESIAN_POINT('',(-30.,600.5,11.5000000000007));
#5545=CARTESIAN_POINT('Origin',(30.,600.5,11.5000000000007));
#5546=CARTESIAN_POINT('',(25.,730.5,11.5000000000007));
#5547=CARTESIAN_POINT('',(30.,730.5,11.5000000000007));
#5548=CARTESIAN_POINT('',(25.,600.5,11.5000000000007));
#5549=CARTESIAN_POINT('Origin',(25.,600.5,16.5000000000007));
#5550=CARTESIAN_POINT('',(30.,730.5,16.5000000000007));
#5551=CARTESIAN_POINT('Origin',(25.,730.5,16.5000000000007));
#5552=CARTESIAN_POINT('',(30.,600.5,16.5000000000007));
#5553=CARTESIAN_POINT('Origin',(-25.,600.5,66.5000000000007));
#5554=CARTESIAN_POINT('',(-25.,730.5,71.5000000000007));
#5555=CARTESIAN_POINT('',(-30.,730.5,66.5000000000007));
#5556=CARTESIAN_POINT('Origin',(-25.,730.5,66.5000000000007));
#5557=CARTESIAN_POINT('',(-30.,600.5,66.5000000000007));
#5558=CARTESIAN_POINT('',(-25.,600.5,71.5000000000007));
#5559=CARTESIAN_POINT('Origin',(-30.,600.5,71.5000000000007));
#5560=CARTESIAN_POINT('',(25.,730.5,71.5000000000007));
#5561=CARTESIAN_POINT('',(25.,600.5,71.5000000000007));
#5562=CARTESIAN_POINT('',(-30.,730.5,71.5000000000007));
#5563=CARTESIAN_POINT('Origin',(25.,600.5,66.5000000000007));
#5564=CARTESIAN_POINT('',(30.,730.5,66.5000000000007));
#5565=CARTESIAN_POINT('Origin',(25.,730.5,66.5000000000007));
#5566=CARTESIAN_POINT('',(30.,600.5,66.5000000000007));
#5567=CARTESIAN_POINT('Origin',(30.,600.5,71.5000000000007));
#5568=CARTESIAN_POINT('',(30.,730.5,71.5000000000007));
#5569=CARTESIAN_POINT('Origin',(-30.,600.5,11.5000000000007));
#5570=CARTESIAN_POINT('',(-30.,730.5,11.5000000000007));
#5571=CARTESIAN_POINT('Origin',(0.,730.5,41.5000000000007));
#6075=UNCERTAINTY_MEASURE_WITH_UNIT(LENGTH_MEASURE(0.01),#6097,
'DISTANCE_ACCURACY_VALUE',
'Maximum model space distance between geometric entities at asserted c
onnectivities');
#6083=UNCERTAINTY_MEASURE_WITH_UNIT(LENGTH_MEASURE(0.01),#6097,
'DISTANCE_ACCURACY_VALUE',
'Maximum model space distance between geometric entities at asserted c
onnectivities');
#6088=(
GEOMETRIC_REPRESENTATION_CONTEXT(3)
GLOBAL_UNCERTAINTY_ASSIGNED_CONTEXT((#6075))
GLOBAL_UNIT_ASSIGNED_CONTEXT((#6097,#6099,#6100))
REPRESENTATION_CONTEXT('','3D')
);
#6096=(
GEOMETRIC_REPRESENTATION_CONTEXT(3)
GLOBAL_UNCERTAINTY_ASSIGNED_CONTEXT((#6083))
GLOBAL_UNIT_ASSIGNED_CONTEXT((#6097,#6099,#6100))
REPRESENTATION_CONTEXT('','3D')
);
#6097=(
LENGTH_UNIT()
NAMED_UNIT(*)
SI_UNIT(.MILLI.,.METRE.)
);
#6099=(
NAMED_UNIT(*)
PLANE_ANGLE_UNIT()
SI_UNIT($,.RADIAN.)
);
#6100=(
NAMED_UNIT(*)
SI_UNIT($,.STERADIAN.)
SOLID_ANGLE_UNIT()
);
#6105=SHAPE_DEFINITION_REPRESENTATION(#6117,#6140);
#6117=PRODUCT_DEFINITION_SHAPE('',$,#6153);
#6140=SHAPE_REPRESENTATION('',(#3856),#6088);
#6148=PRODUCT_DEFINITION_CONTEXT('part definition',#6186,'design');
#6153=PRODUCT_DEFINITION('Motor','Motor',#6165,#6148);
#6165=PRODUCT_DEFINITION_FORMATION('',$,#6192);
#6186=APPLICATION_CONTEXT(
'Core Data for Automotive Mechanical Design Process');
#6187=PRODUCT_CONTEXT('part definition',#6186,'mechanical');
#6192=PRODUCT('Motor','Motor',$,(#6187));
#6263=COLOUR_RGB('Off White',0.89,0.88,0.83);
#6264=FILL_AREA_STYLE_COLOUR('',#6263);
#6265=FILL_AREA_STYLE('',(#6264));
#6266=SURFACE_STYLE_FILL_AREA(#6265);
#6267=SURFACE_SIDE_STYLE('',(#6266));
#6268=SURFACE_STYLE_USAGE(.BOTH.,#6267);
#6269=PRESENTATION_STYLE_ASSIGNMENT((#6268));
ENDSEC;
END-ISO-10303-21;
